ISO-10303-21;
HEADER;
FILE_DESCRIPTION (('STEP AP214'),
    '1' );
FILE_NAME ('Part4.step',
    '2026-11-01T05:08:46',
    ( '' ),
    ( '' ),
    'SwSTEP 2.0',
    'SolidWorks 2024',
    '' );
FILE_SCHEMA (( 'AUTOMOTIVE_DESIGN' ));
ENDSEC;

DATA;
#31=CARTESIAN_POINT ( 'NONE',  ( 0.000000000000000000, 381.0487089519837127, -150.0000000000032685 ) ) ;
#59=EDGE_CURVE ( 'NONE', #4001, #7250, #15126, .T. ) ;
#125=AXIS2_PLACEMENT_3D ( 'NONE', #6705, #364, #11958 ) ;
#128=FACE_BOUND ( 'NONE', #8268, .T. ) ;
#133=DIRECTION ( 'NONE',  ( 0.000000000000000000, 1.000000000000000000, 7.137148015447440312E-15 ) ) ;
#139=VECTOR ( 'NONE', #7023, 1000.000000000000000 ) ;
#140=CARTESIAN_POINT ( 'NONE',  ( 0.000000000000000000, 372.8685141053778693, -83.18019484660869978 ) ) ;
#171=ADVANCED_FACE ( 'NONE', ( #7019, #14589, #1619, #3175, #12191, #9441 ), #16134, .T. ) ;
#176=AXIS2_PLACEMENT_3D ( 'NONE', #3692, #15697, #1104 ) ;
#190=DIRECTION ( 'NONE',  ( 0.000000000000000000, 0.000000000000000000, 1.000000000000000000 ) ) ;
#204=VERTEX_POINT ( 'NONE', #1798 ) ;
#206=DIRECTION ( 'NONE',  ( 0.000000000000000000, 0.000000000000000000, -1.000000000000000000 ) ) ;
#239=EDGE_LOOP ( 'NONE', ( #5498, #1229, #14459, #13552 ) ) ;
#258=CARTESIAN_POINT ( 'NONE',  ( 10.00000000000000000, 372.8685141053778693, -86.48019484660871115 ) ) ;
#263=EDGE_CURVE ( 'NONE', #2860, #5863, #1951, .T. ) ;
#271=CYLINDRICAL_SURFACE ( 'NONE', #4773, 4.999999999999990230 ) ;
#355=AXIS2_PLACEMENT_3D ( 'NONE', #13041, #9260, #1093 ) ;
#362=CIRCLE ( 'NONE', #9957, 3.300000000000011369 ) ;
#364=DIRECTION ( 'NONE',  ( -1.000000000000000000, -0.000000000000000000, -0.000000000000000000 ) ) ;
#375=LINE ( 'NONE', #4332, #16544 ) ;
#419=PLANE ( 'NONE',  #6933 ) ;
#451=ORIENTED_EDGE ( 'NONE', *, *, #16516, .T. ) ;
#520=ORIENTED_EDGE ( 'NONE', *, *, #15915, .F. ) ;
#557=ORIENTED_EDGE ( 'NONE', *, *, #10454, .T. ) ;
#572=VECTOR ( 'NONE', #9766, 1000.000000000000000 ) ;
#610=DIRECTION ( 'NONE',  ( 0.000000000000000000, 0.000000000000000000, 1.000000000000000000 ) ) ;
#660=CIRCLE ( 'NONE', #10797, 5.000000000000004441 ) ;
#685=FACE_OUTER_BOUND ( 'NONE', #4476, .T. ) ;
#689=EDGE_CURVE ( 'NONE', #13804, #2916, #16443, .T. ) ;
#693=AXIS2_PLACEMENT_3D ( 'NONE', #10981, #766, #12520 ) ;
#701=PLANE ( 'NONE',  #3805 ) ;
#717=VERTEX_POINT ( 'NONE', #3483 ) ;
#746=CARTESIAN_POINT ( 'NONE',  ( 0.000000000000000000, 376.0487089519831443, -75.00000000000331113 ) ) ;
#763=CARTESIAN_POINT ( 'NONE',  ( 0.000000000000000000, 306.0487089519832011, -75.00000000000380851 ) ) ;
#766=DIRECTION ( 'NONE',  ( 1.000000000000000000, -0.000000000000000000, 0.000000000000000000 ) ) ;
#767=CARTESIAN_POINT ( 'NONE',  ( 10.00000000000000000, 376.0487089519837127, -150.0000000000033538 ) ) ;
#771=CARTESIAN_POINT ( 'NONE',  ( 10.00000000000000000, 309.2289037985890445, -146.8198051533984199 ) ) ;
#779=DIRECTION ( 'NONE',  ( -1.000000000000000000, -0.000000000000000000, -0.000000000000000000 ) ) ;
#811=ORIENTED_EDGE ( 'NONE', *, *, #3328, .F. ) ;
#875=AXIS2_PLACEMENT_3D ( 'NONE', #6928, #8146, #13397 ) ;
#876=( GEOMETRIC_REPRESENTATION_CONTEXT ( 3 ) GLOBAL_UNCERTAINTY_ASSIGNED_CONTEXT ( ( #4119 ) ) GLOBAL_UNIT_ASSIGNED_CONTEXT ( ( #5895, #12508, #9932 ) ) REPRESENTATION_CONTEXT ( 'NONE', 'WORKASPACE' ) );
#895=LINE ( 'NONE', #8636, #15441 ) ;
#995=ORIENTED_EDGE ( 'NONE', *, *, #8869, .T. ) ;
#1004=VERTEX_POINT ( 'NONE', #14470 ) ;
#1027=AXIS2_PLACEMENT_3D ( 'NONE', #12059, #2774, #16001 ) ;
#1051=ORIENTED_EDGE ( 'NONE', *, *, #8374, .T. ) ;
#1093=DIRECTION ( 'NONE',  ( 0.000000000000000000, 0.000000000000000000, -1.000000000000000000 ) ) ;
#1101=FACE_OUTER_BOUND ( 'NONE', #11342, .T. ) ;
#1104=DIRECTION ( 'NONE',  ( 0.000000000000000000, 0.000000000000000000, -1.000000000000000000 ) ) ;
#1124=DIRECTION ( 'NONE',  ( -1.000000000000000000, -0.000000000000000000, -0.000000000000000000 ) ) ;
#1128=EDGE_CURVE ( 'NONE', #13804, #10865, #16173, .T. ) ;
#1147=ORIENTED_EDGE ( 'NONE', *, *, #9402, .F. ) ;
#1195=LINE ( 'NONE', #6498, #1974 ) ;
#1206=EDGE_CURVE ( 'NONE', #717, #13076, #1195, .T. ) ;
#1207=EDGE_LOOP ( 'NONE', ( #4041, #3316, #12995, #12379, #2271, #520, #2141, #10839 ) ) ;
#1229=ORIENTED_EDGE ( 'NONE', *, *, #16397, .T. ) ;
#1257=LINE ( 'NONE', #16960, #8695 ) ;
#1346=ORIENTED_EDGE ( 'NONE', *, *, #11561, .T. ) ;
#1357=ORIENTED_EDGE ( 'NONE', *, *, #12212, .T. ) ;
#1390=CIRCLE ( 'NONE', #12633, 3.300000000000025135 ) ;
#1462=AXIS2_PLACEMENT_3D ( 'NONE', #6295, #6467, #15664 ) ;
#1488=AXIS2_PLACEMENT_3D ( 'NONE', #3280, #8693, #15217 ) ;
#1502=EDGE_CURVE ( 'NONE', #12140, #1004, #15137, .T. ) ;
#1509=DIRECTION ( 'NONE',  ( 0.000000000000000000, -7.137148015447440312E-15, 1.000000000000000000 ) ) ;
#1521=EDGE_LOOP ( 'NONE', ( #2199, #6012 ) ) ;
#1538=DIRECTION ( 'NONE',  ( 1.000000000000000000, 0.000000000000000000, 0.000000000000000000 ) ) ;
#1560=CYLINDRICAL_SURFACE ( 'NONE', #5660, 3.300000000000011369 ) ;
#1588=( NAMED_UNIT ( * ) PLANE_ANGLE_UNIT ( ) SI_UNIT ( $, .RADIAN. ) );
#1619=FACE_BOUND ( 'NONE', #13605, .T. ) ;
#1639=CARTESIAN_POINT ( 'NONE',  ( 10.00000000000000000, 309.2289037985885898, -83.18019484660915452 ) ) ;
#1655=AXIS2_PLACEMENT_3D ( 'NONE', #15556, #12887, #15805 ) ;
#1684=DIRECTION ( 'NONE',  ( 0.000000000000000000, 0.000000000000000000, -1.000000000000000000 ) ) ;
#1691=CARTESIAN_POINT ( 'NONE',  ( 10.00000000000000000, 372.8685141053783241, -146.8198051533979935 ) ) ;
#1737=ADVANCED_FACE ( 'NONE', ( #4999 ), #6117, .F. ) ;
#1798=CARTESIAN_POINT ( 'NONE',  ( 10.00000000000000000, 341.0487089519837696, -133.5000000000032969 ) ) ;
#1802=ADVANCED_FACE ( 'NONE', ( #4125 ), #15974, .F. ) ;
#1851=VECTOR ( 'NONE', #11286, 1000.000000000000000 ) ;
#1863=CARTESIAN_POINT ( 'NONE',  ( 10.00000000000000000, 309.2289037985885898, -79.88019484660914316 ) ) ;
#1918=EDGE_LOOP ( 'NONE', ( #6102, #11356, #4647, #15464 ) ) ;
#1941=SURFACE_STYLE_USAGE ( .BOTH. , #11218 ) ;
#1951=LINE ( 'NONE', #4783, #6081 ) ;
#1974=VECTOR ( 'NONE', #10387, 1000.000000000000000 ) ;
#1986=DIRECTION ( 'NONE',  ( 0.000000000000000000, 0.000000000000000000, 1.000000000000000000 ) ) ;
#2056=ADVANCED_FACE ( 'NONE', ( #8428 ), #701, .F. ) ;
#2060=EDGE_CURVE ( 'NONE', #3345, #3903, #14866, .T. ) ;
#2141=ORIENTED_EDGE ( 'NONE', *, *, #7590, .F. ) ;
#2199=ORIENTED_EDGE ( 'NONE', *, *, #1502, .T. ) ;
#2214=CARTESIAN_POINT ( 'NONE',  ( 10.00000000000000000, 309.2289037985885898, -83.18019484660915452 ) ) ;
#2227=PRODUCT_CONTEXT ( 'NONE', #4459, 'mechanical' ) ;
#2245=AXIS2_PLACEMENT_3D ( 'NONE', #10314, #10395, #9199 ) ;
#2252=CARTESIAN_POINT ( 'NONE',  ( 10.00000000000000000, 376.0487089519831443, -75.00000000000331113 ) ) ;
#2271=ORIENTED_EDGE ( 'NONE', *, *, #12212, .F. ) ;
#2342=CARTESIAN_POINT ( 'NONE',  ( 10.00000000000000000, 309.2289037985890445, -146.8198051533984199 ) ) ;
#2386=DIRECTION ( 'NONE',  ( 0.000000000000000000, 7.137148015447440312E-15, -1.000000000000000000 ) ) ;
#2395=DIRECTION ( 'NONE',  ( 1.000000000000000000, -0.000000000000000000, 0.000000000000000000 ) ) ;
#2419=SHAPE_REPRESENTATION ( 'Part4', ( #1488 ), #15488 ) ;
#2479=CARTESIAN_POINT ( 'NONE',  ( 0.000000000000000000, 301.0487089519832011, -80.00000000000387956 ) ) ;
#2493=VERTEX_POINT ( 'NONE', #31 ) ;
#2596=ORIENTED_EDGE ( 'NONE', *, *, #10454, .F. ) ;
#2602=DIRECTION ( 'NONE',  ( -1.000000000000000000, -0.000000000000000000, -0.000000000000000000 ) ) ;
#2691=DIRECTION ( 'NONE',  ( 0.000000000000000000, 0.000000000000000000, 1.000000000000000000 ) ) ;
#2748=DIRECTION ( 'NONE',  ( 0.000000000000000000, 0.000000000000000000, -1.000000000000000000 ) ) ;
#2774=DIRECTION ( 'NONE',  ( 1.000000000000000000, -0.000000000000000000, 0.000000000000000000 ) ) ;
#2794=CARTESIAN_POINT ( 'NONE',  ( 0.000000000000000000, 309.2289037985885898, -86.48019484660916589 ) ) ;
#2819=VECTOR ( 'NONE', #3311, 1000.000000000000000 ) ;
#2838=DIRECTION ( 'NONE',  ( -1.000000000000000000, -0.000000000000000000, -0.000000000000000000 ) ) ;
#2860=VERTEX_POINT ( 'NONE', #12561 ) ;
#2892=EDGE_LOOP ( 'NONE', ( #3299, #4726, #14440, #15560 ) ) ;
#2903=VECTOR ( 'NONE', #3461, 1000.000000000000000 ) ;
#2916=VERTEX_POINT ( 'NONE', #14105 ) ;
#2947=ORIENTED_EDGE ( 'NONE', *, *, #16516, .F. ) ;
#2991=ADVANCED_FACE ( 'NONE', ( #6186 ), #11438, .T. ) ;
#2996=DIRECTION ( 'NONE',  ( -1.000000000000000000, -0.000000000000000000, -0.000000000000000000 ) ) ;
#3011=CARTESIAN_POINT ( 'NONE',  ( 0.000000000000000000, 5.352861011586007481E-13, -75.00000000000599698 ) ) ;
#3016=ADVANCED_BREP_SHAPE_REPRESENTATION ( '', ( #14078, #1488 ), #15488 ) ;
#3029=VERTEX_POINT ( 'NONE', #13337 ) ;
#3035=DIRECTION ( 'NONE',  ( 0.000000000000000000, 0.000000000000000000, -1.000000000000000000 ) ) ;
#3037=CARTESIAN_POINT ( 'NONE',  ( 0.000000000000000000, 372.8685141053783241, -150.1198051533980049 ) ) ;
#3091=AXIS2_PLACEMENT_3D ( 'NONE', #6239, #2386, #13989 ) ;
#3175=FACE_BOUND ( 'NONE', #5870, .T. ) ;
#3245=FILL_AREA_STYLE_COLOUR ( '', #16239 ) ;
#3280=CARTESIAN_POINT ( 'NONE',  ( 0.000000000000000000, 0.000000000000000000, 0.000000000000000000 ) ) ;
#3289=ORIENTED_EDGE ( 'NONE', *, *, #9055, .F. ) ;
#3299=ORIENTED_EDGE ( 'NONE', *, *, #1206, .F. ) ;
#3311=DIRECTION ( 'NONE',  ( 0.000000000000000000, 1.000000000000000000, 7.137148015447440312E-15 ) ) ;
#3313=CARTESIAN_POINT ( 'NONE',  ( 0.000000000000000000, 381.0487089519832011, -80.00000000000332534 ) ) ;
#3315=ORIENTED_EDGE ( 'NONE', *, *, #1128, .F. ) ;
#3316=ORIENTED_EDGE ( 'NONE', *, *, #11176, .F. ) ;
#3328=EDGE_CURVE ( 'NONE', #2916, #10595, #16052, .T. ) ;
#3339=CARTESIAN_POINT ( 'NONE',  ( 10.00000000000000000, 309.2289037985890445, -143.5198051533984085 ) ) ;
#3341=AXIS2_PLACEMENT_3D ( 'NONE', #10811, #1538, #6761 ) ;
#3345=VERTEX_POINT ( 'NONE', #9188 ) ;
#3352=DIRECTION ( 'NONE',  ( 0.000000000000000000, -1.000000000000000000, -7.137148015447440312E-15 ) ) ;
#3353=DIRECTION ( 'NONE',  ( -1.000000000000000000, -0.000000000000000000, -0.000000000000000000 ) ) ;
#3430=CARTESIAN_POINT ( 'NONE',  ( 10.00000000000000000, 306.0487089519837696, -155.0000000000038369 ) ) ;
#3441=CYLINDRICAL_SURFACE ( 'NONE', #15530, 3.300000000000025135 ) ;
#3461=DIRECTION ( 'NONE',  ( -1.000000000000000000, -0.000000000000000000, -0.000000000000000000 ) ) ;
#3483=CARTESIAN_POINT ( 'NONE',  ( 10.00000000000000000, 309.2289037985885898, -86.48019484660916589 ) ) ;
#3510=EDGE_CURVE ( 'NONE', #2860, #13804, #13034, .T. ) ;
#3526=LINE ( 'NONE', #8271, #10911 ) ;
#3608=ORIENTED_EDGE ( 'NONE', *, *, #15915, .T. ) ;
#3615=ORIENTED_EDGE ( 'NONE', *, *, #16868, .F. ) ;
#3621=CLOSED_SHELL ( 'NONE', ( #15705, #13817, #1802, #5818, #7108, #2056, #4178, #14957, #10768, #11194, #12314, #10129, #15892, #8156, #6930, #1737, #2991, #171, #8174, #12550 ) ) ;
#3624=EDGE_LOOP ( 'NONE', ( #9559, #5456, #7790, #15729 ) ) ;
#3659=ORIENTED_EDGE ( 'NONE', *, *, #2060, .T. ) ;
#3684=ORIENTED_EDGE ( 'NONE', *, *, #59, .F. ) ;
#3692=CARTESIAN_POINT ( 'NONE',  ( 0.000000000000000000, 309.2289037985885898, -83.18019484660915452 ) ) ;
#3701=AXIS2_PLACEMENT_3D ( 'NONE', #10228, #15467, #3708 ) ;
#3708=DIRECTION ( 'NONE',  ( 0.000000000000000000, 0.000000000000000000, -1.000000000000000000 ) ) ;
#3755=DIRECTION ( 'NONE',  ( 0.000000000000000000, 0.000000000000000000, -1.000000000000000000 ) ) ;
#3784=AXIS2_PLACEMENT_3D ( 'NONE', #767, #15271, #14063 ) ;
#3786=VERTEX_POINT ( 'NONE', #3313 ) ;
#3805=AXIS2_PLACEMENT_3D ( 'NONE', #5922, #7287, #3352 ) ;
#3833=AXIS2_PLACEMENT_3D ( 'NONE', #10701, #5373, #1684 ) ;
#3858=CARTESIAN_POINT ( 'NONE',  ( 10.00000000000000000, 309.2289037985890445, -146.8198051533984199 ) ) ;
#3888=CYLINDRICAL_SURFACE ( 'NONE', #14934, 18.49999999999998934 ) ;
#3903=VERTEX_POINT ( 'NONE', #11043 ) ;
#3910=DIRECTION ( 'NONE',  ( 1.000000000000000000, -0.000000000000000000, 0.000000000000000000 ) ) ;
#4001=VERTEX_POINT ( 'NONE', #16755 ) ;
#4011=LINE ( 'NONE', #13289, #1851 ) ;
#4029=LINE ( 'NONE', #9266, #15091 ) ;
#4041=ORIENTED_EDGE ( 'NONE', *, *, #5442, .F. ) ;
#4054=CIRCLE ( 'NONE', #13659, 3.300000000000025135 ) ;
#4079=DIRECTION ( 'NONE',  ( 0.000000000000000000, 0.000000000000000000, -1.000000000000000000 ) ) ;
#4119=UNCERTAINTY_MEASURE_WITH_UNIT (LENGTH_MEASURE( 1.000000000000000082E-05 ), #5895, 'distance_accuracy_value', 'NONE');
#4125=FACE_OUTER_BOUND ( 'NONE', #6213, .T. ) ;
#4143=ORIENTED_EDGE ( 'NONE', *, *, #6557, .T. ) ;
#4150=CARTESIAN_POINT ( 'NONE',  ( 10.00000000000000000, 372.8685141053778693, -83.18019484660869978 ) ) ;
#4178=ADVANCED_FACE ( 'NONE', ( #13246 ), #12124, .T. ) ;
#4200=CARTESIAN_POINT ( 'NONE',  ( 10.00000000000000000, 376.0487089519837127, -155.0000000000033253 ) ) ;
#4221=CIRCLE ( 'NONE', #8610, 3.300000000000011369 ) ;
#4278=VERTEX_POINT ( 'NONE', #15037 ) ;
#4287=ORIENTED_EDGE ( 'NONE', *, *, #14755, .F. ) ;
#4332=CARTESIAN_POINT ( 'NONE',  ( 10.00000000000000000, 372.8685141053783241, -150.1198051533980049 ) ) ;
#4336=ORIENTED_EDGE ( 'NONE', *, *, #12710, .T. ) ;
#4369=CARTESIAN_POINT ( 'NONE',  ( 10.00000000000000000, 306.0487089519832011, -80.00000000000380851 ) ) ;
#4383=LINE ( 'NONE', #258, #16317 ) ;
#4394=CARTESIAN_POINT ( 'NONE',  ( 10.00000000000000000, 309.2289037985885898, -83.18019484660915452 ) ) ;
#4414=VERTEX_POINT ( 'NONE', #2479 ) ;
#4418=CARTESIAN_POINT ( 'NONE',  ( 10.00000000000000000, 306.0487089519837696, -155.0000000000038369 ) ) ;
#4446=EDGE_CURVE ( 'NONE', #15081, #2860, #9192, .T. ) ;
#4459=APPLICATION_CONTEXT ( 'automotive_design' ) ;
#4476=EDGE_LOOP ( 'NONE', ( #10747, #8446, #9392, #13016 ) ) ;
#4482=CIRCLE ( 'NONE', #3701, 18.49999999999998934 ) ;
#4488=EDGE_CURVE ( 'NONE', #14135, #7845, #4383, .T. ) ;
#4517=CARTESIAN_POINT ( 'NONE',  ( 10.00000000000000000, 306.0487089519832011, -75.00000000000380851 ) ) ;
#4520=DIRECTION ( 'NONE',  ( 1.000000000000000000, -0.000000000000000000, 0.000000000000000000 ) ) ;
#4521=CARTESIAN_POINT ( 'NONE',  ( 10.00000000000000000, 1.106257942394396377E-12, -155.0000000000060254 ) ) ;
#4606=FILL_AREA_STYLE ('',( #3245 ) ) ;
#4626=CARTESIAN_POINT ( 'NONE',  ( 10.00000000000000000, 372.8685141053778693, -83.18019484660869978 ) ) ;
#4639=CARTESIAN_POINT ( 'NONE',  ( 10.00000000000000000, 372.8685141053783241, -146.8198051533979935 ) ) ;
#4647=ORIENTED_EDGE ( 'NONE', *, *, #8562, .F. ) ;
#4677=ORIENTED_EDGE ( 'NONE', *, *, #9286, .F. ) ;
#4726=ORIENTED_EDGE ( 'NONE', *, *, #11407, .T. ) ;
#4733=EDGE_CURVE ( 'NONE', #4278, #12140, #12524, .T. ) ;
#4759=LINE ( 'NONE', #1863, #5477 ) ;
#4773=AXIS2_PLACEMENT_3D ( 'NONE', #9365, #2838, #16150 ) ;
#4780=AXIS2_PLACEMENT_3D ( 'NONE', #13111, #12847, #3755 ) ;
#4783=CARTESIAN_POINT ( 'NONE',  ( 10.00000000000000000, 301.0487089519837127, -150.0000000000038369 ) ) ;
#4884=CARTESIAN_POINT ( 'NONE',  ( 10.00000000000000000, 372.8685141053783241, -146.8198051533979935 ) ) ;
#4905=DIRECTION ( 'NONE',  ( -1.000000000000000000, -0.000000000000000000, -0.000000000000000000 ) ) ;
#4999=FACE_OUTER_BOUND ( 'NONE', #239, .T. ) ;
#5042=DIRECTION ( 'NONE',  ( 0.000000000000000000, 0.000000000000000000, -1.000000000000000000 ) ) ;
#5051=PRODUCT_DEFINITION_SHAPE ( 'NONE', 'NONE',  #13142 ) ;
#5167=ORIENTED_EDGE ( 'NONE', *, *, #7802, .F. ) ;
#5183=DIRECTION ( 'NONE',  ( 0.000000000000000000, 0.000000000000000000, -1.000000000000000000 ) ) ;
#5261=VERTEX_POINT ( 'NONE', #8731 ) ;
#5266=VECTOR ( 'NONE', #2996, 1000.000000000000000 ) ;
#5321=UNCERTAINTY_MEASURE_WITH_UNIT (LENGTH_MEASURE( 1.000000000000000082E-05 ), #15914, 'distance_accuracy_value', 'NONE');
#5351=FACE_OUTER_BOUND ( 'NONE', #1207, .T. ) ;
#5373=DIRECTION ( 'NONE',  ( 1.000000000000000000, -0.000000000000000000, 0.000000000000000000 ) ) ;
#5426=DIRECTION ( 'NONE',  ( 1.000000000000000000, 0.000000000000000000, 0.000000000000000000 ) ) ;
#5442=EDGE_CURVE ( 'NONE', #10865, #10595, #5523, .T. ) ;
#5456=ORIENTED_EDGE ( 'NONE', *, *, #6557, .F. ) ;
#5477=VECTOR ( 'NONE', #10014, 1000.000000000000000 ) ;
#5495=ORIENTED_EDGE ( 'NONE', *, *, #11827, .T. ) ;
#5498=ORIENTED_EDGE ( 'NONE', *, *, #8340, .F. ) ;
#5501=EDGE_CURVE ( 'NONE', #7500, #4414, #5647, .T. ) ;
#5514=PLANE ( 'NONE',  #1027 ) ;
#5523=LINE ( 'NONE', #13013, #7554 ) ;
#5526=MECHANICAL_DESIGN_GEOMETRIC_PRESENTATION_REPRESENTATION('',(#16497),#876);
#5530=PLANE ( 'NONE',  #11547 ) ;
#5554=DIRECTION ( 'NONE',  ( 1.000000000000000000, -0.000000000000000000, 0.000000000000000000 ) ) ;
#5571=CIRCLE ( 'NONE', #13256, 3.300000000000025135 ) ;
#5611=DIRECTION ( 'NONE',  ( -1.000000000000000000, -0.000000000000000000, -0.000000000000000000 ) ) ;
#5644=DIRECTION ( 'NONE',  ( 0.000000000000000000, -1.000000000000000000, -7.137148015447440312E-15 ) ) ;
#5647=CIRCLE ( 'NONE', #7828, 4.999999999999990230 ) ;
#5660=AXIS2_PLACEMENT_3D ( 'NONE', #4394, #13667, #9632 ) ;
#5666=ORIENTED_EDGE ( 'NONE', *, *, #9402, .T. ) ;
#5673=CARTESIAN_POINT ( 'NONE',  ( 0.000000000000000000, 372.8685141053778693, -83.18019484660869978 ) ) ;
#5818=ADVANCED_FACE ( 'NONE', ( #16398 ), #9717, .F. ) ;
#5841=EDGE_CURVE ( 'NONE', #9546, #717, #14716, .T. ) ;
#5863=VERTEX_POINT ( 'NONE', #12368 ) ;
#5870=EDGE_LOOP ( 'NONE', ( #15585, #6628 ) ) ;
#5873=AXIS2_PLACEMENT_3D ( 'NONE', #4639, #15044, #1986 ) ;
#5895=( LENGTH_UNIT ( ) NAMED_UNIT ( * ) SI_UNIT ( .MILLI., .METRE. ) );
#5922=CARTESIAN_POINT ( 'NONE',  ( 10.00000000000000000, 1.106257942394396377E-12, -155.0000000000060254 ) ) ;
#5941=CARTESIAN_POINT ( 'NONE',  ( 0.000000000000000000, 376.0487089519832011, -80.00000000000332534 ) ) ;
#5958=LINE ( 'NONE', #16761, #8055 ) ;
#6012=ORIENTED_EDGE ( 'NONE', *, *, #11673, .T. ) ;
#6081=VECTOR ( 'NONE', #7267, 1000.000000000000000 ) ;
#6092=CIRCLE ( 'NONE', #355, 3.300000000000011369 ) ;
#6102=ORIENTED_EDGE ( 'NONE', *, *, #16637, .T. ) ;
#6114=AXIS2_PLACEMENT_3D ( 'NONE', #16671, #4905, #10155 ) ;
#6117=CYLINDRICAL_SURFACE ( 'NONE', #14779, 3.300000000000025135 ) ;
#6147=CIRCLE ( 'NONE', #14117, 3.300000000000025135 ) ;
#6163=ORIENTED_EDGE ( 'NONE', *, *, #12151, .F. ) ;
#6186=FACE_OUTER_BOUND ( 'NONE', #13690, .T. ) ;
#6213=EDGE_LOOP ( 'NONE', ( #8966, #9474, #4287, #3289 ) ) ;
#6239=CARTESIAN_POINT ( 'NONE',  ( 10.00000000000000000, 5.352861011586007481E-13, -75.00000000000599698 ) ) ;
#6242=DIRECTION ( 'NONE',  ( 0.000000000000000000, 0.000000000000000000, -1.000000000000000000 ) ) ;
#6256=CYLINDRICAL_SURFACE ( 'NONE', #2245, 5.000000000000004441 ) ;
#6295=CARTESIAN_POINT ( 'NONE',  ( 10.00000000000000000, 372.8685141053778693, -83.18019484660869978 ) ) ;
#6299=CIRCLE ( 'NONE', #1655, 3.300000000000025135 ) ;
#6307=EDGE_LOOP ( 'NONE', ( #8253, #7647, #451, #2596 ) ) ;
#6393=ORIENTED_EDGE ( 'NONE', *, *, #4488, .F. ) ;
#6404=ORIENTED_EDGE ( 'NONE', *, *, #9934, .T. ) ;
#6444=CARTESIAN_POINT ( 'NONE',  ( 10.00000000000000000, 381.0487089519832011, -80.00000000000332534 ) ) ;
#6450=EDGE_LOOP ( 'NONE', ( #9272, #5495 ) ) ;
#6467=DIRECTION ( 'NONE',  ( 1.000000000000000000, -0.000000000000000000, 0.000000000000000000 ) ) ;
#6471=CARTESIAN_POINT ( 'NONE',  ( 0.000000000000000000, 309.2289037985890445, -146.8198051533984199 ) ) ;
#6498=CARTESIAN_POINT ( 'NONE',  ( 10.00000000000000000, 309.2289037985885898, -86.48019484660916589 ) ) ;
#6499=ORIENTED_EDGE ( 'NONE', *, *, #16397, .F. ) ;
#6506=VERTEX_POINT ( 'NONE', #3037 ) ;
#6557=EDGE_CURVE ( 'NONE', #10409, #3786, #12814, .T. ) ;
#6560=DIRECTION ( 'NONE',  ( 0.000000000000000000, -7.137148015447440312E-15, 1.000000000000000000 ) ) ;
#6584=ORIENTED_EDGE ( 'NONE', *, *, #11176, .T. ) ;
#6622=CYLINDRICAL_SURFACE ( 'NONE', #8436, 3.300000000000011369 ) ;
#6628=ORIENTED_EDGE ( 'NONE', *, *, #10323, .F. ) ;
#6642=CARTESIAN_POINT ( 'NONE',  ( 0.000000000000000000, 376.0487089519837127, -150.0000000000033538 ) ) ;
#6687=CIRCLE ( 'NONE', #16303, 5.000000000000004441 ) ;
#6696=DIRECTION ( 'NONE',  ( -1.000000000000000000, -0.000000000000000000, -0.000000000000000000 ) ) ;
#6705=CARTESIAN_POINT ( 'NONE',  ( 10.00000000000000000, 376.0487089519837127, -150.0000000000033538 ) ) ;
#6744=ORIENTED_EDGE ( 'NONE', *, *, #16868, .T. ) ;
#6761=DIRECTION ( 'NONE',  ( 0.000000000000000000, 0.000000000000000000, -1.000000000000000000 ) ) ;
#6848=CIRCLE ( 'NONE', #3833, 3.300000000000025135 ) ;
#6883=FACE_BOUND ( 'NONE', #12535, .T. ) ;
#6889=( NAMED_UNIT ( * ) SI_UNIT ( $, .STERADIAN. ) SOLID_ANGLE_UNIT ( ) );
#6928=CARTESIAN_POINT ( 'NONE',  ( 10.00000000000000000, 0.000000000000000000, 0.000000000000000000 ) ) ;
#6930=ADVANCED_FACE ( 'NONE', ( #8077 ), #1560, .F. ) ;
#6933=AXIS2_PLACEMENT_3D ( 'NONE', #9693, #5644, #14839 ) ;
#7008=PRODUCT ( 'Part4', 'Part4', '', ( #2227 ) ) ;
#7010=DIRECTION ( 'NONE',  ( 1.000000000000000000, -0.000000000000000000, 0.000000000000000000 ) ) ;
#7019=FACE_BOUND ( 'NONE', #11134, .T. ) ;
#7023=DIRECTION ( 'NONE',  ( -1.000000000000000000, -0.000000000000000000, -0.000000000000000000 ) ) ;
#7045=EDGE_LOOP ( 'NONE', ( #1357, #6163, #9198, #12871 ) ) ;
#7046=CARTESIAN_POINT ( 'NONE',  ( 0.000000000000000000, 372.8685141053783241, -143.5198051533979537 ) ) ;
#7048=DIRECTION ( 'NONE',  ( 1.000000000000000000, -0.000000000000000000, -0.000000000000000000 ) ) ;
#7108=ADVANCED_FACE ( 'NONE', ( #16652 ), #3441, .F. ) ;
#7111=EDGE_LOOP ( 'NONE', ( #12385, #811, #8622, #13646 ) ) ;
#7127=DIRECTION ( 'NONE',  ( 1.000000000000000000, -0.000000000000000000, 0.000000000000000000 ) ) ;
#7149=CARTESIAN_POINT ( 'NONE',  ( 10.00000000000000000, 381.0487089519837127, -150.0000000000032685 ) ) ;
#7162=PRESENTATION_STYLE_ASSIGNMENT (( #1941 ) ) ;
#7232=ORIENTED_EDGE ( 'NONE', *, *, #4446, .F. ) ;
#7250=VERTEX_POINT ( 'NONE', #7789 ) ;
#7259=CARTESIAN_POINT ( 'NONE',  ( 0.000000000000000000, 341.0487089519837696, -115.0000000000032969 ) ) ;
#7267=DIRECTION ( 'NONE',  ( -1.000000000000000000, -0.000000000000000000, -0.000000000000000000 ) ) ;
#7274=EDGE_CURVE ( 'NONE', #13076, #8177, #14984, .T. ) ;
#7287=DIRECTION ( 'NONE',  ( 0.000000000000000000, -7.137148015447440312E-15, 1.000000000000000000 ) ) ;
#7291=AXIS2_PLACEMENT_3D ( 'NONE', #4626, #16474, #10046 ) ;
#7343=DIRECTION ( 'NONE',  ( 0.000000000000000000, 0.000000000000000000, -1.000000000000000000 ) ) ;
#7370=CARTESIAN_POINT ( 'NONE',  ( 10.00000000000000000, 372.8685141053783241, -146.8198051533979935 ) ) ;
#7500=VERTEX_POINT ( 'NONE', #763 ) ;
#7540=DIRECTION ( 'NONE',  ( 0.000000000000000000, 0.000000000000000000, -1.000000000000000000 ) ) ;
#7554=VECTOR ( 'NONE', #133, 1000.000000000000000 ) ;
#7590=EDGE_CURVE ( 'NONE', #2493, #3786, #1257, .T. ) ;
#7637=LINE ( 'NONE', #12889, #11890 ) ;
#7647=ORIENTED_EDGE ( 'NONE', *, *, #7775, .T. ) ;
#7761=ORIENTED_EDGE ( 'NONE', *, *, #5841, .F. ) ;
#7775=EDGE_CURVE ( 'NONE', #7250, #13244, #4011, .T. ) ;
#7789=CARTESIAN_POINT ( 'NONE',  ( 0.000000000000000000, 341.0487089519837696, -96.50000000000331113 ) ) ;
#7790=ORIENTED_EDGE ( 'NONE', *, *, #12710, .F. ) ;
#7802=EDGE_CURVE ( 'NONE', #10409, #15631, #16905, .T. ) ;
#7828=AXIS2_PLACEMENT_3D ( 'NONE', #15838, #9238, #4079 ) ;
#7832=ORIENTED_EDGE ( 'NONE', *, *, #263, .F. ) ;
#7845=VERTEX_POINT ( 'NONE', #12412 ) ;
#7910=DIRECTION ( 'NONE',  ( 1.000000000000000000, -0.000000000000000000, -0.000000000000000000 ) ) ;
#7988=AXIS2_PLACEMENT_3D ( 'NONE', #8794, #8536, #11274 ) ;
#8005=CARTESIAN_POINT ( 'NONE',  ( 0.000000000000000000, 309.2289037985885898, -79.88019484660914316 ) ) ;
#8055=VECTOR ( 'NONE', #2602, 1000.000000000000000 ) ;
#8063=AXIS2_PLACEMENT_3D ( 'NONE', #7259, #13130, #6242 ) ;
#8077=FACE_OUTER_BOUND ( 'NONE', #2892, .T. ) ;
#8106=VERTEX_POINT ( 'NONE', #14469 ) ;
#8146=DIRECTION ( 'NONE',  ( 1.000000000000000000, -0.000000000000000000, 0.000000000000000000 ) ) ;
#8156=ADVANCED_FACE ( 'NONE', ( #9393 ), #6622, .F. ) ;
#8174=ADVANCED_FACE ( 'NONE', ( #11885, #8188, #128, #10763, #6883, #5351 ), #5514, .F. ) ;
#8177=VERTEX_POINT ( 'NONE', #8005 ) ;
#8185=ORIENTED_EDGE ( 'NONE', *, *, #15158, .T. ) ;
#8188=FACE_BOUND ( 'NONE', #1521, .T. ) ;
#8193=SHAPE_REPRESENTATION_RELATIONSHIP ( 'NONE' , 'NONE' ,  #2419, #3016 ) ;
#8253=ORIENTED_EDGE ( 'NONE', *, *, #11827, .F. ) ;
#8268=EDGE_LOOP ( 'NONE', ( #14224, #11629 ) ) ;
#8271=CARTESIAN_POINT ( 'NONE',  ( 10.00000000000000000, 309.2289037985890445, -150.1198051533984597 ) ) ;
#8300=EDGE_CURVE ( 'NONE', #8106, #5261, #14193, .T. ) ;
#8308=AXIS2_PLACEMENT_3D ( 'NONE', #4369, #11451, #11277 ) ;
#8340=EDGE_CURVE ( 'NONE', #3029, #1004, #3526, .T. ) ;
#8374=EDGE_CURVE ( 'NONE', #15631, #13257, #15455, .T. ) ;
#8397=ORIENTED_EDGE ( 'NONE', *, *, #4488, .T. ) ;
#8416=EDGE_CURVE ( 'NONE', #4278, #3029, #4054, .T. ) ;
#8428=FACE_OUTER_BOUND ( 'NONE', #7111, .T. ) ;
#8436=AXIS2_PLACEMENT_3D ( 'NONE', #4150, #5611, #2691 ) ;
#8446=ORIENTED_EDGE ( 'NONE', *, *, #8340, .T. ) ;
#8507=ORIENTED_EDGE ( 'NONE', *, *, #11444, .F. ) ;
#8518=DIRECTION ( 'NONE',  ( 0.000000000000000000, 0.000000000000000000, -1.000000000000000000 ) ) ;
#8526=ORIENTED_EDGE ( 'NONE', *, *, #16123, .T. ) ;
#8536=DIRECTION ( 'NONE',  ( 1.000000000000000000, -0.000000000000000000, 0.000000000000000000 ) ) ;
#8539=LINE ( 'NONE', #13779, #13555 ) ;
#8562=EDGE_CURVE ( 'NONE', #2916, #11402, #11185, .T. ) ;
#8565=ORIENTED_EDGE ( 'NONE', *, *, #2060, .F. ) ;
#8566=AXIS2_PLACEMENT_3D ( 'NONE', #6471, #9247, #5183 ) ;
#8594=CARTESIAN_POINT ( 'NONE',  ( 10.00000000000000000, 372.8685141053778693, -79.88019484660868841 ) ) ;
#8610=AXIS2_PLACEMENT_3D ( 'NONE', #5673, #14699, #2748 ) ;
#8622=ORIENTED_EDGE ( 'NONE', *, *, #689, .F. ) ;
#8636=CARTESIAN_POINT ( 'NONE',  ( 0.000000000000000000, 301.0487089519826327, 2.148629195649657075E-12 ) ) ;
#8668=DIRECTION ( 'NONE',  ( -1.000000000000000000, -0.000000000000000000, -0.000000000000000000 ) ) ;
#8693=DIRECTION ( 'NONE',  ( 0.000000000000000000, 0.000000000000000000, 1.000000000000000000 ) ) ;
#8695=VECTOR ( 'NONE', #6560, 1000.000000000000000 ) ;
#8721=DIRECTION ( 'NONE',  ( -1.000000000000000000, -0.000000000000000000, -0.000000000000000000 ) ) ;
#8731=CARTESIAN_POINT ( 'NONE',  ( 10.00000000000000000, 372.8685141053783241, -143.5198051533979537 ) ) ;
#8768=SHAPE_DEFINITION_REPRESENTATION ( #5051, #2419 ) ;
#8794=CARTESIAN_POINT ( 'NONE',  ( 10.00000000000000000, 372.8685141053778693, -83.18019484660869978 ) ) ;
#8807=ORIENTED_EDGE ( 'NONE', *, *, #263, .T. ) ;
#8826=VECTOR ( 'NONE', #7048, 1000.000000000000000 ) ;
#8834=PLANE ( 'NONE',  #3091 ) ;
#8845=DIRECTION ( 'NONE',  ( -1.000000000000000000, -0.000000000000000000, -0.000000000000000000 ) ) ;
#8855=CARTESIAN_POINT ( 'NONE',  ( 0.000000000000000000, 306.0487089519837696, -155.0000000000038369 ) ) ;
#8869=EDGE_CURVE ( 'NONE', #6506, #13502, #6848, .T. ) ;
#8873=CIRCLE ( 'NONE', #1462, 3.300000000000011369 ) ;
#8876=VECTOR ( 'NONE', #13417, 1000.000000000000000 ) ;
#8941=FACE_OUTER_BOUND ( 'NONE', #9908, .T. ) ;
#8966=ORIENTED_EDGE ( 'NONE', *, *, #5841, .T. ) ;
#9007=VERTEX_POINT ( 'NONE', #746 ) ;
#9018=CARTESIAN_POINT ( 'NONE',  ( 10.00000000000000000, 5.352861011586007481E-13, -75.00000000000599698 ) ) ;
#9055=EDGE_CURVE ( 'NONE', #9546, #8177, #4759, .T. ) ;
#9128=CARTESIAN_POINT ( 'NONE',  ( 0.000000000000000000, 341.0487089519837696, -115.0000000000032969 ) ) ;
#9188=CARTESIAN_POINT ( 'NONE',  ( 10.00000000000000000, 372.8685141053778693, -79.88019484660868841 ) ) ;
#9192=LINE ( 'NONE', #12879, #11639 ) ;
#9198=ORIENTED_EDGE ( 'NONE', *, *, #8374, .F. ) ;
#9199=DIRECTION ( 'NONE',  ( 0.000000000000000000, 0.000000000000000000, 1.000000000000000000 ) ) ;
#9238=DIRECTION ( 'NONE',  ( 1.000000000000000000, -0.000000000000000000, 0.000000000000000000 ) ) ;
#9247=DIRECTION ( 'NONE',  ( 1.000000000000000000, -0.000000000000000000, 0.000000000000000000 ) ) ;
#9256=AXIS2_PLACEMENT_3D ( 'NONE', #12329, #4520, #11126 ) ;
#9260=DIRECTION ( 'NONE',  ( 1.000000000000000000, -0.000000000000000000, 0.000000000000000000 ) ) ;
#9266=CARTESIAN_POINT ( 'NONE',  ( 10.00000000000000000, 381.0487089519826895, 2.719601036885452502E-12 ) ) ;
#9272=ORIENTED_EDGE ( 'NONE', *, *, #59, .T. ) ;
#9282=LINE ( 'NONE', #3011, #8876 ) ;
#9286=EDGE_CURVE ( 'NONE', #5261, #13502, #10857, .T. ) ;
#9303=CARTESIAN_POINT ( 'NONE',  ( 0.000000000000000000, 309.2289037985890445, -146.8198051533984199 ) ) ;
#9346=DIRECTION ( 'NONE',  ( 0.000000000000000000, -7.137148015447440312E-15, 1.000000000000000000 ) ) ;
#9365=CARTESIAN_POINT ( 'NONE',  ( 10.00000000000000000, 306.0487089519832011, -80.00000000000380851 ) ) ;
#9392=ORIENTED_EDGE ( 'NONE', *, *, #1502, .F. ) ;
#9393=FACE_OUTER_BOUND ( 'NONE', #12905, .T. ) ;
#9402=EDGE_CURVE ( 'NONE', #13502, #6506, #6299, .T. ) ;
#9419=CIRCLE ( 'NONE', #9695, 18.49999999999998934 ) ;
#9441=FACE_OUTER_BOUND ( 'NONE', #13426, .T. ) ;
#9474=ORIENTED_EDGE ( 'NONE', *, *, #1206, .T. ) ;
#9541=VECTOR ( 'NONE', #11756, 1000.000000000000000 ) ;
#9546=VERTEX_POINT ( 'NONE', #12723 ) ;
#9559=ORIENTED_EDGE ( 'NONE', *, *, #7590, .T. ) ;
#9561=CARTESIAN_POINT ( 'NONE',  ( 0.000000000000000000, 341.0487089519837696, -133.5000000000032969 ) ) ;
#9564=DIRECTION ( 'NONE',  ( -1.000000000000000000, -0.000000000000000000, -0.000000000000000000 ) ) ;
#9598=FACE_OUTER_BOUND ( 'NONE', #3624, .T. ) ;
#9632=DIRECTION ( 'NONE',  ( 0.000000000000000000, 0.000000000000000000, 1.000000000000000000 ) ) ;
#9658=DIRECTION ( 'NONE',  ( -1.000000000000000000, -0.000000000000000000, -0.000000000000000000 ) ) ;
#9693=CARTESIAN_POINT ( 'NONE',  ( 10.00000000000000000, 381.0487089519826895, 2.719601036885452502E-12 ) ) ;
#9695=AXIS2_PLACEMENT_3D ( 'NONE', #16253, #5426, #3035 ) ;
#9707=EDGE_CURVE ( 'NONE', #5261, #8106, #1390, .T. ) ;
#9717=CYLINDRICAL_SURFACE ( 'NONE', #7291, 3.300000000000011369 ) ;
#9766=DIRECTION ( 'NONE',  ( -1.000000000000000000, -0.000000000000000000, -0.000000000000000000 ) ) ;
#9908=EDGE_LOOP ( 'NONE', ( #3608, #16724, #5167, #4143 ) ) ;
#9918=LINE ( 'NONE', #7149, #572 ) ;
#9932=( NAMED_UNIT ( * ) SI_UNIT ( $, .STERADIAN. ) SOLID_ANGLE_UNIT ( ) );
#9934=EDGE_CURVE ( 'NONE', #3903, #7845, #14576, .T. ) ;
#9957=AXIS2_PLACEMENT_3D ( 'NONE', #16043, #5554, #14761 ) ;
#10014=DIRECTION ( 'NONE',  ( -1.000000000000000000, -0.000000000000000000, -0.000000000000000000 ) ) ;
#10042=DIRECTION ( 'NONE',  ( 0.000000000000000000, 0.000000000000000000, 1.000000000000000000 ) ) ;
#10046=DIRECTION ( 'NONE',  ( 0.000000000000000000, 0.000000000000000000, 1.000000000000000000 ) ) ;
#10074=ORIENTED_EDGE ( 'NONE', *, *, #10323, .T. ) ;
#10129=ADVANCED_FACE ( 'NONE', ( #16181 ), #5530, .F. ) ;
#10155=DIRECTION ( 'NONE',  ( 0.000000000000000000, 0.000000000000000000, 1.000000000000000000 ) ) ;
#10228=CARTESIAN_POINT ( 'NONE',  ( 10.00000000000000000, 341.0487089519837696, -115.0000000000032969 ) ) ;
#10314=CARTESIAN_POINT ( 'NONE',  ( 10.00000000000000000, 376.0487089519832011, -80.00000000000332534 ) ) ;
#10323=EDGE_CURVE ( 'NONE', #14135, #3345, #15680, .T. ) ;
#10387=DIRECTION ( 'NONE',  ( -1.000000000000000000, -0.000000000000000000, -0.000000000000000000 ) ) ;
#10390=VECTOR ( 'NONE', #779, 1000.000000000000000 ) ;
#10395=DIRECTION ( 'NONE',  ( -1.000000000000000000, -0.000000000000000000, -0.000000000000000000 ) ) ;
#10409=VERTEX_POINT ( 'NONE', #6444 ) ;
#10425=ORIENTED_EDGE ( 'NONE', *, *, #16123, .F. ) ;
#10454=EDGE_CURVE ( 'NONE', #4001, #204, #15823, .T. ) ;
#10489=ORIENTED_EDGE ( 'NONE', *, *, #3510, .F. ) ;
#10510=DIRECTION ( 'NONE',  ( -1.000000000000000000, -0.000000000000000000, -0.000000000000000000 ) ) ;
#10595=VERTEX_POINT ( 'NONE', #16338 ) ;
#10614=DIRECTION ( 'NONE',  ( 0.000000000000000000, 0.000000000000000000, -1.000000000000000000 ) ) ;
#10701=CARTESIAN_POINT ( 'NONE',  ( 0.000000000000000000, 372.8685141053783241, -146.8198051533979935 ) ) ;
#10747=ORIENTED_EDGE ( 'NONE', *, *, #8416, .T. ) ;
#10763=FACE_BOUND ( 'NONE', #14312, .T. ) ;
#10768=ADVANCED_FACE ( 'NONE', ( #8941 ), #6256, .T. ) ;
#10776=EDGE_LOOP ( 'NONE', ( #15253, #14816 ) ) ;
#10778=CARTESIAN_POINT ( 'NONE',  ( 10.00000000000000000, 301.0487089519826327, 2.148629195649657075E-12 ) ) ;
#10797=AXIS2_PLACEMENT_3D ( 'NONE', #6642, #11993, #10614 ) ;
#10804=CARTESIAN_POINT ( 'NONE',  ( 10.00000000000000000, 381.0487089519837127, -150.0000000000032685 ) ) ;
#10811=CARTESIAN_POINT ( 'NONE',  ( 0.000000000000000000, 341.0487089519837696, -115.0000000000032969 ) ) ;
#10820=PRODUCT_DEFINITION_FORMATION_WITH_SPECIFIED_SOURCE ( 'ANY', '', #7008, .NOT_KNOWN. ) ;
#10839=ORIENTED_EDGE ( 'NONE', *, *, #16637, .F. ) ;
#10857=LINE ( 'NONE', #16095, #15372 ) ;
#10865=VERTEX_POINT ( 'NONE', #8855 ) ;
#10911=VECTOR ( 'NONE', #8845, 1000.000000000000000 ) ;
#10981=CARTESIAN_POINT ( 'NONE',  ( 10.00000000000000000, 306.0487089519837127, -150.0000000000038369 ) ) ;
#11043=CARTESIAN_POINT ( 'NONE',  ( 0.000000000000000000, 372.8685141053778693, -79.88019484660868841 ) ) ;
#11052=DIRECTION ( 'NONE',  ( 0.000000000000000000, 0.000000000000000000, -1.000000000000000000 ) ) ;
#11054=ORIENTED_EDGE ( 'NONE', *, *, #11891, .F. ) ;
#11108=EDGE_LOOP ( 'NONE', ( #14959, #14493, #1147, #4677 ) ) ;
#11126=DIRECTION ( 'NONE',  ( 0.000000000000000000, 0.000000000000000000, -1.000000000000000000 ) ) ;
#11134=EDGE_LOOP ( 'NONE', ( #10425, #2947 ) ) ;
#11156=CYLINDRICAL_SURFACE ( 'NONE', #13439, 3.300000000000025135 ) ;
#11176=EDGE_CURVE ( 'NONE', #5863, #10865, #11585, .T. ) ;
#11180=CYLINDRICAL_SURFACE ( 'NONE', #5873, 3.300000000000025135 ) ;
#11184=ORIENTED_EDGE ( 'NONE', *, *, #8562, .T. ) ;
#11185=CIRCLE ( 'NONE', #3784, 5.000000000000004441 ) ;
#11188=ORIENTED_EDGE ( 'NONE', *, *, #3510, .T. ) ;
#11194=ADVANCED_FACE ( 'NONE', ( #12789 ), #8834, .F. ) ;
#11218=SURFACE_SIDE_STYLE ('',( #13716 ) ) ;
#11223=CARTESIAN_POINT ( 'NONE',  ( 10.00000000000000000, 309.2289037985890445, -146.8198051533984199 ) ) ;
#11274=DIRECTION ( 'NONE',  ( 0.000000000000000000, 0.000000000000000000, -1.000000000000000000 ) ) ;
#11277=DIRECTION ( 'NONE',  ( 0.000000000000000000, 0.000000000000000000, -1.000000000000000000 ) ) ;
#11280=AXIS2_PLACEMENT_3D ( 'NONE', #140, #3910, #11641 ) ;
#11286=DIRECTION ( 'NONE',  ( 1.000000000000000000, -0.000000000000000000, -0.000000000000000000 ) ) ;
#11342=EDGE_LOOP ( 'NONE', ( #15983, #3684, #557, #8526 ) ) ;
#11356=ORIENTED_EDGE ( 'NONE', *, *, #13198, .F. ) ;
#11392=DIRECTION ( 'NONE',  ( 1.000000000000000000, -0.000000000000000000, 0.000000000000000000 ) ) ;
#11402=VERTEX_POINT ( 'NONE', #10804 ) ;
#11407=EDGE_CURVE ( 'NONE', #717, #9546, #362, .T. ) ;
#11438=CYLINDRICAL_SURFACE ( 'NONE', #6114, 5.000000000000004441 ) ;
#11444=EDGE_CURVE ( 'NONE', #13257, #15081, #13533, .T. ) ;
#11451=DIRECTION ( 'NONE',  ( 1.000000000000000000, -0.000000000000000000, 0.000000000000000000 ) ) ;
#11474=APPLICATION_CONTEXT ( 'automotive_design' ) ;
#11506=ORIENTED_EDGE ( 'NONE', *, *, #9286, .T. ) ;
#11547=AXIS2_PLACEMENT_3D ( 'NONE', #10778, #13281, #1509 ) ;
#11561=EDGE_CURVE ( 'NONE', #4414, #5863, #895, .T. ) ;
#11585=CIRCLE ( 'NONE', #12697, 5.000000000000004441 ) ;
#11629=ORIENTED_EDGE ( 'NONE', *, *, #7274, .T. ) ;
#11639=VECTOR ( 'NONE', #14426, 1000.000000000000000 ) ;
#11641=DIRECTION ( 'NONE',  ( 0.000000000000000000, 0.000000000000000000, -1.000000000000000000 ) ) ;
#11673=EDGE_CURVE ( 'NONE', #1004, #12140, #5571, .T. ) ;
#11722=AXIS2_PLACEMENT_3D ( 'NONE', #7370, #15369, #7540 ) ;
#11756=DIRECTION ( 'NONE',  ( 0.000000000000000000, -1.000000000000000000, -7.137148015447440312E-15 ) ) ;
#11787=DIRECTION ( 'NONE',  ( 0.000000000000000000, 0.000000000000000000, -1.000000000000000000 ) ) ;
#11827=EDGE_CURVE ( 'NONE', #7250, #4001, #9419, .T. ) ;
#11852=CARTESIAN_POINT ( 'NONE',  ( 0.000000000000000000, 309.2289037985890445, -143.5198051533984085 ) ) ;
#11857=ORIENTED_EDGE ( 'NONE', *, *, #11407, .F. ) ;
#11885=FACE_BOUND ( 'NONE', #6450, .T. ) ;
#11890=VECTOR ( 'NONE', #1124, 1000.000000000000000 ) ;
#11891=EDGE_CURVE ( 'NONE', #8106, #6506, #375, .T. ) ;
#11958=DIRECTION ( 'NONE',  ( 0.000000000000000000, 0.000000000000000000, 1.000000000000000000 ) ) ;
#11965=AXIS2_PLACEMENT_3D ( 'NONE', #2214, #12702, #16319 ) ;
#11993=DIRECTION ( 'NONE',  ( 1.000000000000000000, -0.000000000000000000, 0.000000000000000000 ) ) ;
#12059=CARTESIAN_POINT ( 'NONE',  ( 0.000000000000000000, 0.000000000000000000, 0.000000000000000000 ) ) ;
#12124=CYLINDRICAL_SURFACE ( 'NONE', #125, 5.000000000000004441 ) ;
#12140=VERTEX_POINT ( 'NONE', #11852 ) ;
#12151=EDGE_CURVE ( 'NONE', #13257, #7500, #7637, .T. ) ;
#12191=FACE_BOUND ( 'NONE', #10776, .T. ) ;
#12212=EDGE_CURVE ( 'NONE', #9007, #7500, #9282, .T. ) ;
#12255=EDGE_CURVE ( 'NONE', #7845, #3903, #4221, .T. ) ;
#12271=ORIENTED_EDGE ( 'NONE', *, *, #4446, .T. ) ;
#12314=ADVANCED_FACE ( 'NONE', ( #13236 ), #271, .T. ) ;
#12329=CARTESIAN_POINT ( 'NONE',  ( 10.00000000000000000, 376.0487089519832011, -80.00000000000332534 ) ) ;
#12368=CARTESIAN_POINT ( 'NONE',  ( 0.000000000000000000, 301.0487089519837127, -150.0000000000038369 ) ) ;
#12379=ORIENTED_EDGE ( 'NONE', *, *, #5501, .F. ) ;
#12385=ORIENTED_EDGE ( 'NONE', *, *, #5442, .T. ) ;
#12412=CARTESIAN_POINT ( 'NONE',  ( 0.000000000000000000, 372.8685141053778693, -86.48019484660871115 ) ) ;
#12508=( NAMED_UNIT ( * ) PLANE_ANGLE_UNIT ( ) SI_UNIT ( $, .RADIAN. ) );
#12520=DIRECTION ( 'NONE',  ( 0.000000000000000000, 0.000000000000000000, -1.000000000000000000 ) ) ;
#12524=LINE ( 'NONE', #3339, #139 ) ;
#12535=EDGE_LOOP ( 'NONE', ( #5666, #995 ) ) ;
#12550=ADVANCED_FACE ( 'NONE', ( #1101 ), #15696, .F. ) ;
#12561=CARTESIAN_POINT ( 'NONE',  ( 10.00000000000000000, 301.0487089519837127, -150.0000000000038369 ) ) ;
#12613=ORIENTED_EDGE ( 'NONE', *, *, #8300, .T. ) ;
#12633=AXIS2_PLACEMENT_3D ( 'NONE', #1691, #7010, #11052 ) ;
#12656=DIRECTION ( 'NONE',  ( 0.000000000000000000, 7.137148015447440312E-15, -1.000000000000000000 ) ) ;
#12697=AXIS2_PLACEMENT_3D ( 'NONE', #15443, #16721, #5042 ) ;
#12702=DIRECTION ( 'NONE',  ( 1.000000000000000000, -0.000000000000000000, 0.000000000000000000 ) ) ;
#12710=EDGE_CURVE ( 'NONE', #11402, #10409, #4029, .T. ) ;
#12723=CARTESIAN_POINT ( 'NONE',  ( 10.00000000000000000, 309.2289037985885898, -79.88019484660914316 ) ) ;
#12724=EDGE_LOOP ( 'NONE', ( #13119, #3615, #8507, #15566 ) ) ;
#12789=FACE_OUTER_BOUND ( 'NONE', #7045, .T. ) ;
#12814=LINE ( 'NONE', #16669, #2903 ) ;
#12847=DIRECTION ( 'NONE',  ( 1.000000000000000000, 0.000000000000000000, 0.000000000000000000 ) ) ;
#12871=ORIENTED_EDGE ( 'NONE', *, *, #15591, .T. ) ;
#12879=CARTESIAN_POINT ( 'NONE',  ( 10.00000000000000000, 301.0487089519826327, 2.148629195649657075E-12 ) ) ;
#12887=DIRECTION ( 'NONE',  ( 1.000000000000000000, -0.000000000000000000, 0.000000000000000000 ) ) ;
#12889=CARTESIAN_POINT ( 'NONE',  ( 10.00000000000000000, 306.0487089519832011, -75.00000000000380851 ) ) ;
#12905=EDGE_LOOP ( 'NONE', ( #6393, #10074, #3659, #13800 ) ) ;
#12995=ORIENTED_EDGE ( 'NONE', *, *, #11561, .F. ) ;
#13013=CARTESIAN_POINT ( 'NONE',  ( 0.000000000000000000, 1.106257942394396377E-12, -155.0000000000060254 ) ) ;
#13016=ORIENTED_EDGE ( 'NONE', *, *, #4733, .F. ) ;
#13034=CIRCLE ( 'NONE', #693, 5.000000000000004441 ) ;
#13036=ORIENTED_EDGE ( 'NONE', *, *, #8869, .F. ) ;
#13041=CARTESIAN_POINT ( 'NONE',  ( 0.000000000000000000, 309.2289037985885898, -83.18019484660915452 ) ) ;
#13076=VERTEX_POINT ( 'NONE', #2794 ) ;
#13087=FACE_OUTER_BOUND ( 'NONE', #6307, .T. ) ;
#13089=DIRECTION ( 'NONE',  ( 1.000000000000000000, -0.000000000000000000, 0.000000000000000000 ) ) ;
#13111=CARTESIAN_POINT ( 'NONE',  ( 10.00000000000000000, 341.0487089519837696, -115.0000000000032969 ) ) ;
#13119=ORIENTED_EDGE ( 'NONE', *, *, #5501, .T. ) ;
#13130=DIRECTION ( 'NONE',  ( 1.000000000000000000, -0.000000000000000000, -0.000000000000000000 ) ) ;
#13142=PRODUCT_DEFINITION ( 'UNKNOWN', '', #10820, #13581 ) ;
#13167=EDGE_LOOP ( 'NONE', ( #8185, #8397, #14980, #8565 ) ) ;
#13198=EDGE_CURVE ( 'NONE', #11402, #2493, #9918, .T. ) ;
#13236=FACE_OUTER_BOUND ( 'NONE', #12724, .T. ) ;
#13244=VERTEX_POINT ( 'NONE', #16279 ) ;
#13246=FACE_OUTER_BOUND ( 'NONE', #1918, .T. ) ;
#13256=AXIS2_PLACEMENT_3D ( 'NONE', #9303, #13089, #11787 ) ;
#13257=VERTEX_POINT ( 'NONE', #4517 ) ;
#13262=VECTOR ( 'NONE', #9658, 1000.000000000000000 ) ;
#13281=DIRECTION ( 'NONE',  ( -0.000000000000000000, 1.000000000000000000, 7.137148015447440312E-15 ) ) ;
#13289=CARTESIAN_POINT ( 'NONE',  ( 0.000000000000000000, 341.0487089519837696, -96.50000000000331113 ) ) ;
#13320=DIRECTION ( 'NONE',  ( -1.000000000000000000, -0.000000000000000000, -0.000000000000000000 ) ) ;
#13337=CARTESIAN_POINT ( 'NONE',  ( 10.00000000000000000, 309.2289037985890445, -150.1198051533984597 ) ) ;
#13397=DIRECTION ( 'NONE',  ( 0.000000000000000000, 0.000000000000000000, -1.000000000000000000 ) ) ;
#13417=DIRECTION ( 'NONE',  ( 0.000000000000000000, -1.000000000000000000, -7.137148015447440312E-15 ) ) ;
#13426=EDGE_LOOP ( 'NONE', ( #15052, #11184, #4336, #15422, #1051, #14358, #12271, #11188 ) ) ;
#13439=AXIS2_PLACEMENT_3D ( 'NONE', #771, #8668, #10042 ) ;
#13502=VERTEX_POINT ( 'NONE', #7046 ) ;
#13533=CIRCLE ( 'NONE', #8308, 4.999999999999990230 ) ;
#13552=ORIENTED_EDGE ( 'NONE', *, *, #11673, .F. ) ;
#13555=VECTOR ( 'NONE', #8721, 1000.000000000000000 ) ;
#13581=PRODUCT_DEFINITION_CONTEXT ( 'detailed design', #11474, 'design' ) ;
#13605=EDGE_LOOP ( 'NONE', ( #7761, #11857 ) ) ;
#13646=ORIENTED_EDGE ( 'NONE', *, *, #1128, .T. ) ;
#13659=AXIS2_PLACEMENT_3D ( 'NONE', #3858, #2395, #16900 ) ;
#13667=DIRECTION ( 'NONE',  ( -1.000000000000000000, -0.000000000000000000, -0.000000000000000000 ) ) ;
#13690=EDGE_LOOP ( 'NONE', ( #6584, #3315, #10489, #8807 ) ) ;
#13716=SURFACE_STYLE_FILL_AREA ( #4606 ) ;
#13779=CARTESIAN_POINT ( 'NONE',  ( 10.00000000000000000, 301.0487089519832011, -80.00000000000387956 ) ) ;
#13800=ORIENTED_EDGE ( 'NONE', *, *, #12255, .F. ) ;
#13804=VERTEX_POINT ( 'NONE', #3430 ) ;
#13817=ADVANCED_FACE ( 'NONE', ( #685 ), #11156, .F. ) ;
#13989=DIRECTION ( 'NONE',  ( 0.000000000000000000, 1.000000000000000000, 7.137148015447440312E-15 ) ) ;
#14063=DIRECTION ( 'NONE',  ( 0.000000000000000000, 0.000000000000000000, -1.000000000000000000 ) ) ;
#14078=MANIFOLD_SOLID_BREP ( 'Cut-Extrude1', #3621 ) ;
#14105=CARTESIAN_POINT ( 'NONE',  ( 10.00000000000000000, 376.0487089519837127, -155.0000000000033253 ) ) ;
#14117=AXIS2_PLACEMENT_3D ( 'NONE', #11223, #11392, #7343 ) ;
#14135=VERTEX_POINT ( 'NONE', #15514 ) ;
#14193=CIRCLE ( 'NONE', #11722, 3.300000000000025135 ) ;
#14224=ORIENTED_EDGE ( 'NONE', *, *, #14755, .T. ) ;
#14312=EDGE_LOOP ( 'NONE', ( #6404, #15306 ) ) ;
#14358=ORIENTED_EDGE ( 'NONE', *, *, #11444, .T. ) ;
#14420=EDGE_LOOP ( 'NONE', ( #11054, #12613, #11506, #13036 ) ) ;
#14426=DIRECTION ( 'NONE',  ( 0.000000000000000000, 7.137148015447440312E-15, -1.000000000000000000 ) ) ;
#14440=ORIENTED_EDGE ( 'NONE', *, *, #9055, .T. ) ;
#14459=ORIENTED_EDGE ( 'NONE', *, *, #4733, .T. ) ;
#14469=CARTESIAN_POINT ( 'NONE',  ( 10.00000000000000000, 372.8685141053783241, -150.1198051533980049 ) ) ;
#14470=CARTESIAN_POINT ( 'NONE',  ( 0.000000000000000000, 309.2289037985890445, -150.1198051533984597 ) ) ;
#14493=ORIENTED_EDGE ( 'NONE', *, *, #11891, .T. ) ;
#14576=CIRCLE ( 'NONE', #11280, 3.300000000000011369 ) ;
#14589=FACE_BOUND ( 'NONE', #16596, .T. ) ;
#14699=DIRECTION ( 'NONE',  ( 1.000000000000000000, -0.000000000000000000, 0.000000000000000000 ) ) ;
#14716=CIRCLE ( 'NONE', #11965, 3.300000000000011369 ) ;
#14755=EDGE_CURVE ( 'NONE', #8177, #13076, #6092, .T. ) ;
#14761=DIRECTION ( 'NONE',  ( 0.000000000000000000, 0.000000000000000000, -1.000000000000000000 ) ) ;
#14779=AXIS2_PLACEMENT_3D ( 'NONE', #2342, #16604, #16435 ) ;
#14816=ORIENTED_EDGE ( 'NONE', *, *, #8300, .F. ) ;
#14839=DIRECTION ( 'NONE',  ( 0.000000000000000000, 7.137148015447440312E-15, -1.000000000000000000 ) ) ;
#14866=LINE ( 'NONE', #8594, #10390 ) ;
#14934=AXIS2_PLACEMENT_3D ( 'NONE', #9128, #7910, #206 ) ;
#14957=ADVANCED_FACE ( 'NONE', ( #9598 ), #419, .F. ) ;
#14959=ORIENTED_EDGE ( 'NONE', *, *, #9707, .T. ) ;
#14971=FACE_OUTER_BOUND ( 'NONE', #14420, .T. ) ;
#14980=ORIENTED_EDGE ( 'NONE', *, *, #9934, .F. ) ;
#14984=CIRCLE ( 'NONE', #176, 3.300000000000011369 ) ;
#15037=CARTESIAN_POINT ( 'NONE',  ( 10.00000000000000000, 309.2289037985890445, -143.5198051533984085 ) ) ;
#15044=DIRECTION ( 'NONE',  ( -1.000000000000000000, -0.000000000000000000, -0.000000000000000000 ) ) ;
#15052=ORIENTED_EDGE ( 'NONE', *, *, #689, .T. ) ;
#15081=VERTEX_POINT ( 'NONE', #16295 ) ;
#15091=VECTOR ( 'NONE', #9346, 1000.000000000000000 ) ;
#15126=CIRCLE ( 'NONE', #3341, 18.49999999999998934 ) ;
#15137=CIRCLE ( 'NONE', #8566, 3.300000000000025135 ) ;
#15158=EDGE_CURVE ( 'NONE', #3345, #14135, #8873, .T. ) ;
#15202=EDGE_LOOP ( 'NONE', ( #1346, #7832, #7232, #6744 ) ) ;
#15215=CIRCLE ( 'NONE', #4780, 18.49999999999998934 ) ;
#15217=DIRECTION ( 'NONE',  ( 1.000000000000000000, 0.000000000000000000, 0.000000000000000000 ) ) ;
#15253=ORIENTED_EDGE ( 'NONE', *, *, #9707, .F. ) ;
#15271=DIRECTION ( 'NONE',  ( 1.000000000000000000, -0.000000000000000000, 0.000000000000000000 ) ) ;
#15306=ORIENTED_EDGE ( 'NONE', *, *, #12255, .T. ) ;
#15311=AXIS2_PLACEMENT_3D ( 'NONE', #1639, #6696, #190 ) ;
#15369=DIRECTION ( 'NONE',  ( 1.000000000000000000, -0.000000000000000000, 0.000000000000000000 ) ) ;
#15372=VECTOR ( 'NONE', #10510, 1000.000000000000000 ) ;
#15422=ORIENTED_EDGE ( 'NONE', *, *, #7802, .T. ) ;
#15441=VECTOR ( 'NONE', #12656, 1000.000000000000000 ) ;
#15443=CARTESIAN_POINT ( 'NONE',  ( 0.000000000000000000, 306.0487089519837127, -150.0000000000038369 ) ) ;
#15455=LINE ( 'NONE', #9018, #9541 ) ;
#15464=ORIENTED_EDGE ( 'NONE', *, *, #3328, .T. ) ;
#15467=DIRECTION ( 'NONE',  ( 1.000000000000000000, 0.000000000000000000, 0.000000000000000000 ) ) ;
#15488=( GEOMETRIC_REPRESENTATION_CONTEXT ( 3 ) GLOBAL_UNCERTAINTY_ASSIGNED_CONTEXT ( ( #5321 ) ) GLOBAL_UNIT_ASSIGNED_CONTEXT ( ( #15914, #1588, #6889 ) ) REPRESENTATION_CONTEXT ( 'NONE', 'WORKASPACE' ) );
#15503=ORIENTED_EDGE ( 'NONE', *, *, #8416, .F. ) ;
#15514=CARTESIAN_POINT ( 'NONE',  ( 10.00000000000000000, 372.8685141053778693, -86.48019484660871115 ) ) ;
#15530=AXIS2_PLACEMENT_3D ( 'NONE', #4884, #3353, #610 ) ;
#15556=CARTESIAN_POINT ( 'NONE',  ( 0.000000000000000000, 372.8685141053783241, -146.8198051533979935 ) ) ;
#15560=ORIENTED_EDGE ( 'NONE', *, *, #7274, .F. ) ;
#15566=ORIENTED_EDGE ( 'NONE', *, *, #12151, .T. ) ;
#15585=ORIENTED_EDGE ( 'NONE', *, *, #15158, .F. ) ;
#15591=EDGE_CURVE ( 'NONE', #15631, #9007, #5958, .T. ) ;
#15631=VERTEX_POINT ( 'NONE', #2252 ) ;
#15664=DIRECTION ( 'NONE',  ( 0.000000000000000000, 0.000000000000000000, -1.000000000000000000 ) ) ;
#15680=CIRCLE ( 'NONE', #7988, 3.300000000000011369 ) ;
#15696=CYLINDRICAL_SURFACE ( 'NONE', #8063, 18.49999999999998934 ) ;
#15697=DIRECTION ( 'NONE',  ( 1.000000000000000000, -0.000000000000000000, 0.000000000000000000 ) ) ;
#15705=ADVANCED_FACE ( 'NONE', ( #13087 ), #3888, .F. ) ;
#15729=ORIENTED_EDGE ( 'NONE', *, *, #13198, .T. ) ;
#15805=DIRECTION ( 'NONE',  ( 0.000000000000000000, 0.000000000000000000, -1.000000000000000000 ) ) ;
#15823=LINE ( 'NONE', #9561, #8826 ) ;
#15838=CARTESIAN_POINT ( 'NONE',  ( 0.000000000000000000, 306.0487089519832011, -80.00000000000380851 ) ) ;
#15892=ADVANCED_FACE ( 'NONE', ( #14971 ), #11180, .F. ) ;
#15914=( LENGTH_UNIT ( ) NAMED_UNIT ( * ) SI_UNIT ( .MILLI., .METRE. ) );
#15915=EDGE_CURVE ( 'NONE', #3786, #9007, #6687, .T. ) ;
#15974=CYLINDRICAL_SURFACE ( 'NONE', #15311, 3.300000000000011369 ) ;
#15983=ORIENTED_EDGE ( 'NONE', *, *, #7775, .F. ) ;
#16001=DIRECTION ( 'NONE',  ( 0.000000000000000000, 0.000000000000000000, -1.000000000000000000 ) ) ;
#16043=CARTESIAN_POINT ( 'NONE',  ( 10.00000000000000000, 309.2289037985885898, -83.18019484660915452 ) ) ;
#16052=LINE ( 'NONE', #4200, #5266 ) ;
#16095=CARTESIAN_POINT ( 'NONE',  ( 10.00000000000000000, 372.8685141053783241, -143.5198051533979537 ) ) ;
#16123=EDGE_CURVE ( 'NONE', #204, #13244, #4482, .T. ) ;
#16134=PLANE ( 'NONE',  #875 ) ;
#16150=DIRECTION ( 'NONE',  ( 0.000000000000000000, 0.000000000000000000, 1.000000000000000000 ) ) ;
#16173=LINE ( 'NONE', #4418, #13262 ) ;
#16181=FACE_OUTER_BOUND ( 'NONE', #15202, .T. ) ;
#16239=COLOUR_RGB ( '', 0.66274510, 0.83137255, 0.94901961) ;
#16253=CARTESIAN_POINT ( 'NONE',  ( 0.000000000000000000, 341.0487089519837696, -115.0000000000032969 ) ) ;
#16279=CARTESIAN_POINT ( 'NONE',  ( 10.00000000000000000, 341.0487089519837696, -96.50000000000331113 ) ) ;
#16295=CARTESIAN_POINT ( 'NONE',  ( 10.00000000000000000, 301.0487089519832011, -80.00000000000387956 ) ) ;
#16303=AXIS2_PLACEMENT_3D ( 'NONE', #5941, #7127, #8518 ) ;
#16317=VECTOR ( 'NONE', #13320, 1000.000000000000000 ) ;
#16319=DIRECTION ( 'NONE',  ( 0.000000000000000000, 0.000000000000000000, -1.000000000000000000 ) ) ;
#16338=CARTESIAN_POINT ( 'NONE',  ( 0.000000000000000000, 376.0487089519837127, -155.0000000000033253 ) ) ;
#16397=EDGE_CURVE ( 'NONE', #3029, #4278, #6147, .T. ) ;
#16398=FACE_OUTER_BOUND ( 'NONE', #13167, .T. ) ;
#16435=DIRECTION ( 'NONE',  ( 0.000000000000000000, 0.000000000000000000, 1.000000000000000000 ) ) ;
#16443=LINE ( 'NONE', #4521, #2819 ) ;
#16474=DIRECTION ( 'NONE',  ( -1.000000000000000000, -0.000000000000000000, -0.000000000000000000 ) ) ;
#16497=STYLED_ITEM ( 'NONE', ( #7162 ), #14078 ) ;
#16516=EDGE_CURVE ( 'NONE', #13244, #204, #15215, .T. ) ;
#16544=VECTOR ( 'NONE', #9564, 1000.000000000000000 ) ;
#16596=EDGE_LOOP ( 'NONE', ( #15503, #6499 ) ) ;
#16604=DIRECTION ( 'NONE',  ( -1.000000000000000000, -0.000000000000000000, -0.000000000000000000 ) ) ;
#16637=EDGE_CURVE ( 'NONE', #10595, #2493, #660, .T. ) ;
#16652=FACE_OUTER_BOUND ( 'NONE', #11108, .T. ) ;
#16669=CARTESIAN_POINT ( 'NONE',  ( 10.00000000000000000, 381.0487089519832011, -80.00000000000332534 ) ) ;
#16671=CARTESIAN_POINT ( 'NONE',  ( 10.00000000000000000, 306.0487089519837127, -150.0000000000038369 ) ) ;
#16721=DIRECTION ( 'NONE',  ( 1.000000000000000000, -0.000000000000000000, 0.000000000000000000 ) ) ;
#16724=ORIENTED_EDGE ( 'NONE', *, *, #15591, .F. ) ;
#16755=CARTESIAN_POINT ( 'NONE',  ( 0.000000000000000000, 341.0487089519837696, -133.5000000000032969 ) ) ;
#16761=CARTESIAN_POINT ( 'NONE',  ( 10.00000000000000000, 376.0487089519831443, -75.00000000000331113 ) ) ;
#16868=EDGE_CURVE ( 'NONE', #15081, #4414, #8539, .T. ) ;
#16900=DIRECTION ( 'NONE',  ( 0.000000000000000000, 0.000000000000000000, -1.000000000000000000 ) ) ;
#16905=CIRCLE ( 'NONE', #9256, 5.000000000000004441 ) ;
#16960=CARTESIAN_POINT ( 'NONE',  ( 0.000000000000000000, 381.0487089519826895, 2.719601036885452502E-12 ) ) ;
ENDSEC;
END-ISO-10303-21;
